ISO-10303-21;
HEADER;
FILE_DESCRIPTION (('STEP AP203'),
    '1' );
FILE_NAME ('1602p_c_14.step',
    '2026-10-31T14:11:27',
    ( '' ),
    ( '' ),
    'SwSTEP 2.0',
    'SolidWorks 2024',
    '' );
FILE_SCHEMA (( 'AUTOMOTIVE_DESIGN' ));
ENDSEC;

DATA;
#130=CARTESIAN_POINT ( 'NONE',  ( -22.49917142882856069, 22.89791325974001879, 4.999999999999900524 ) ) ;
#161=DIRECTION ( 'NONE',  ( -2.982858504489129897E-17, 2.441916418604790135E-15, 1.000000000000000000 ) ) ;
#210=( GEOMETRIC_REPRESENTATION_CONTEXT ( 3 ) GLOBAL_UNCERTAINTY_ASSIGNED_CONTEXT ( ( #9838 ) ) GLOBAL_UNIT_ASSIGNED_CONTEXT ( ( #2432, #18585, #11238 ) ) REPRESENTATION_CONTEXT ( 'NONE', 'WORKASPACE' ) );
#262=DIRECTION ( 'NONE',  ( -0.9997651245102238127, -0.02167246670447303680, 0.000000000000000000 ) ) ;
#415=DIRECTION ( 'NONE',  ( 1.000000000000000000, 0.000000000000000000, 0.000000000000000000 ) ) ;
#532=EDGE_LOOP ( 'NONE', ( #10638, #21531, #13593, #19724 ) ) ;
#576=PRODUCT ( '1602p_c_14', '1602p_c_14', '', ( #2740 ) ) ;
#887=CARTESIAN_POINT ( 'NONE',  ( -19.99975861755300244, 22.95209442650120124, 4.999999999999900524 ) ) ;
#1250=EDGE_LOOP ( 'NONE', ( #1501, #11961, #11225, #22871 ) ) ;
#1284=ADVANCED_FACE ( 'NONE', ( #3836 ), #2062, .T. ) ;
#1501=ORIENTED_EDGE ( 'NONE', *, *, #20404, .T. ) ;
#1537=ORIENTED_EDGE ( 'NONE', *, *, #16483, .T. ) ;
#1608=VERTEX_POINT ( 'NONE', #5137 ) ;
#1750=VERTEX_POINT ( 'NONE', #130 ) ;
#2062=CYLINDRICAL_SURFACE ( 'NONE', #14308, 3.500000000000001332 ) ;
#2174=CARTESIAN_POINT ( 'NONE',  ( -19.99975861755300244, 22.95209442650120124, 3.749999999999900080 ) ) ;
#2188=CARTESIAN_POINT ( 'NONE',  ( -16.50058068176721804, 23.02794805996685668, 4.999999999999900524 ) ) ;
#2298=SHAPE_REPRESENTATION_RELATIONSHIP ( 'NONE' , 'NONE' ,  #7169, #18164 ) ;
#2358=AXIS2_PLACEMENT_3D ( 'NONE', #22047, #16474, #14590 ) ;
#2383=AXIS2_PLACEMENT_3D ( 'NONE', #887, #13371, #4567 ) ;
#2432=( LENGTH_UNIT ( ) NAMED_UNIT ( * ) SI_UNIT ( .MILLI., .METRE. ) );
#2569=CARTESIAN_POINT ( 'NONE',  ( 0.000000000000000000, 0.000000000000000000, 0.000000000000000000 ) ) ;
#2580=AXIS2_PLACEMENT_3D ( 'NONE', #17763, #21435, #14658 ) ;
#2593=VECTOR ( 'NONE', #5932, 1000.000000000000000 ) ;
#2599=EDGE_CURVE ( 'NONE', #1608, #8149, #11245, .T. ) ;
#2740=MECHANICAL_CONTEXT ( 'NONE', #13089, 'mechanical' ) ;
#2971=ADVANCED_FACE ( 'NONE', ( #10980, #18201 ), #21013, .F. ) ;
#3012=EDGE_CURVE ( 'NONE', #5266, #6885, #22773, .T. ) ;
#3289=AXIS2_PLACEMENT_3D ( 'NONE', #7955, #4738, #15187 ) ;
#3312=EDGE_CURVE ( 'NONE', #10552, #5266, #4814, .T. ) ;
#3546=DIRECTION ( 'NONE',  ( -0.9997651245102238127, -0.02167246670447303680, 0.000000000000000000 ) ) ;
#3652=DIRECTION ( 'NONE',  ( 2.982858504489139758E-17, -2.441916418604790135E-15, -1.000000000000000000 ) ) ;
#3700=CIRCLE ( 'NONE', #16981, 2.500000000000000000 ) ;
#3836=FACE_OUTER_BOUND ( 'NONE', #9931, .T. ) ;
#4382=DIRECTION ( 'NONE',  ( 2.982858504489129897E-17, -2.441916418604790135E-15, -1.000000000000000000 ) ) ;
#4567=DIRECTION ( 'NONE',  ( -0.9997651245102238127, -0.02167246670447303680, 0.000000000000000000 ) ) ;
#4738=DIRECTION ( 'NONE',  ( 2.982858504489129897E-17, -2.441916418604790135E-15, -1.000000000000000000 ) ) ;
#4772=ORIENTED_EDGE ( 'NONE', *, *, #16483, .F. ) ;
#4814=CIRCLE ( 'NONE', #8996, 3.500000000000001332 ) ;
#5137=CARTESIAN_POINT ( 'NONE',  ( -17.50034580627744063, 23.00627559326238369, 4.999999999999900524 ) ) ;
#5266=VERTEX_POINT ( 'NONE', #15789 ) ;
#5471=DIRECTION ( 'NONE',  ( 2.982858504489129897E-17, -2.441916418604790135E-15, -1.000000000000000000 ) ) ;
#5521=CARTESIAN_POINT ( 'NONE',  ( -19.99975861755300244, 22.95209442650120124, 2.499999999999900524 ) ) ;
#5551=VECTOR ( 'NONE', #20768, 1000.000000000000000 ) ;
#5624=DIRECTION ( 'NONE',  ( -0.9997651245102240347, -0.02167246670447264822, 0.000000000000000000 ) ) ;
#5932=DIRECTION ( 'NONE',  ( 2.982858504489129897E-17, -2.441916418604790135E-15, -1.000000000000000000 ) ) ;
#5977=CIRCLE ( 'NONE', #10172, 2.500000000000000000 ) ;
#6047=LINE ( 'NONE', #13300, #2593 ) ;
#6137=ORIENTED_EDGE ( 'NONE', *, *, #13830, .T. ) ;
#6394=CARTESIAN_POINT ( 'NONE',  ( -19.99975861755300244, 22.95209442650120124, 2.499999999999900524 ) ) ;
#6772=DIRECTION ( 'NONE',  ( -0.9997651245102240347, -0.02167246670447264822, 0.000000000000000000 ) ) ;
#6885=VERTEX_POINT ( 'NONE', #19702 ) ;
#6944=CIRCLE ( 'NONE', #2383, 3.500000000000001332 ) ;
#7009=AXIS2_PLACEMENT_3D ( 'NONE', #17802, #16128, #21230 ) ;
#7169=SHAPE_REPRESENTATION ( '1602p_c_14', ( #12739 ), #210 ) ;
#7497=CIRCLE ( 'NONE', #22257, 2.500000000000000000 ) ;
#7546=CLOSED_SHELL ( 'NONE', ( #18101, #12327, #16780, #2971, #1284, #8048 ) ) ;
#7661=PRODUCT_DEFINITION_FORMATION_WITH_SPECIFIED_SOURCE ( 'ANY', '', #576, .NOT_KNOWN. ) ;
#7695=CYLINDRICAL_SURFACE ( 'NONE', #2358, 3.500000000000001332 ) ;
#7955=CARTESIAN_POINT ( 'NONE',  ( -19.99975861755300244, 22.95209442650120124, 4.999999999999900524 ) ) ;
#7968=EDGE_LOOP ( 'NONE', ( #14353, #11779, #11431, #10022 ) ) ;
#8048=ADVANCED_FACE ( 'NONE', ( #12714, #17215 ), #20762, .T. ) ;
#8149=VERTEX_POINT ( 'NONE', #15067 ) ;
#8186=VERTEX_POINT ( 'NONE', #13416 ) ;
#8355=DIRECTION ( 'NONE',  ( -0.9997651245102240347, -0.02167246670447264822, 0.000000000000000000 ) ) ;
#8430=DIRECTION ( 'NONE',  ( 2.982858504489129897E-17, -2.441916418604790135E-15, -1.000000000000000000 ) ) ;
#8487=CARTESIAN_POINT ( 'NONE',  ( -19.99975861755300244, 22.95209442650120124, 2.499999999999900524 ) ) ;
#8996=AXIS2_PLACEMENT_3D ( 'NONE', #18152, #3652, #3546 ) ;
#9038=DIRECTION ( 'NONE',  ( -0.9997651245102238127, -0.02167246670447303680, 0.000000000000000000 ) ) ;
#9123=ORIENTED_EDGE ( 'NONE', *, *, #3012, .T. ) ;
#9169=EDGE_LOOP ( 'NONE', ( #6137, #13080 ) ) ;
#9291=MANIFOLD_SOLID_BREP ( 'Imported1', #7546 ) ;
#9312=DIRECTION ( 'NONE',  ( 2.982858504489139758E-17, -2.441916418604790135E-15, -1.000000000000000000 ) ) ;
#9637=APPLICATION_CONTEXT ( 'configuration controlled 3d designs of mechanical parts and assemblies' ) ;
#9815=EDGE_LOOP ( 'NONE', ( #19202, #15668 ) ) ;
#9838=UNCERTAINTY_MEASURE_WITH_UNIT (LENGTH_MEASURE( 1.000000000000000082E-05 ), #2432, 'distance_accuracy_value', 'NONE');
#9921=DIRECTION ( 'NONE',  ( 2.982858504489129897E-17, -2.441916418604790135E-15, -1.000000000000000000 ) ) ;
#9931=EDGE_LOOP ( 'NONE', ( #20294, #17443, #9123, #1537 ) ) ;
#9999=CYLINDRICAL_SURFACE ( 'NONE', #14142, 2.500000000000000000 ) ;
#10022=ORIENTED_EDGE ( 'NONE', *, *, #11641, .F. ) ;
#10156=DIRECTION ( 'NONE',  ( -2.982858504489129897E-17, 2.441916418604790135E-15, 1.000000000000000000 ) ) ;
#10172=AXIS2_PLACEMENT_3D ( 'NONE', #17955, #5471, #21492 ) ;
#10552=VERTEX_POINT ( 'NONE', #2188 ) ;
#10638=ORIENTED_EDGE ( 'NONE', *, *, #2599, .F. ) ;
#10655=DESIGN_CONTEXT ( 'detailed design', #9637, 'design' ) ;
#10980=FACE_BOUND ( 'NONE', #15628, .T. ) ;
#11000=CYLINDRICAL_SURFACE ( 'NONE', #2580, 2.500000000000000000 ) ;
#11225=ORIENTED_EDGE ( 'NONE', *, *, #18006, .T. ) ;
#11238=( NAMED_UNIT ( * ) SI_UNIT ( $, .STERADIAN. ) SOLID_ANGLE_UNIT ( ) );
#11245=LINE ( 'NONE', #18937, #22994 ) ;
#11431=ORIENTED_EDGE ( 'NONE', *, *, #13830, .F. ) ;
#11506=EDGE_CURVE ( 'NONE', #1750, #1608, #5977, .T. ) ;
#11513=AXIS2_PLACEMENT_3D ( 'NONE', #21842, #14374, #9038 ) ;
#11641=EDGE_CURVE ( 'NONE', #1750, #8186, #6047, .T. ) ;
#11650=DIRECTION ( 'NONE',  ( 9.412241839989958199E-48, -1.000000000000000000, 2.441916418604790135E-15 ) ) ;
#11779=ORIENTED_EDGE ( 'NONE', *, *, #2599, .T. ) ;
#11809=ORIENTED_EDGE ( 'NONE', *, *, #22429, .T. ) ;
#11961=ORIENTED_EDGE ( 'NONE', *, *, #21093, .T. ) ;
#12021=SHAPE_DEFINITION_REPRESENTATION ( #16888, #7169 ) ;
#12254=CIRCLE ( 'NONE', #11513, 3.500000000000001332 ) ;
#12327=ADVANCED_FACE ( 'NONE', ( #14420 ), #11000, .F. ) ;
#12616=EDGE_CURVE ( 'NONE', #8149, #8186, #23412, .T. ) ;
#12714=FACE_BOUND ( 'NONE', #9169, .T. ) ;
#12739=AXIS2_PLACEMENT_3D ( 'NONE', #2569, #13380, #415 ) ;
#12808=FACE_OUTER_BOUND ( 'NONE', #1250, .T. ) ;
#13080=ORIENTED_EDGE ( 'NONE', *, *, #12616, .T. ) ;
#13089=APPLICATION_CONTEXT ( 'configuration controlled 3d designs of mechanical parts and assemblies' ) ;
#13165=PRODUCT_DEFINITION ( 'UNKNOWN', '', #7661, #10655 ) ;
#13234=CARTESIAN_POINT ( 'NONE',  ( -19.99975861755300244, 22.95209442650120124, 4.999999999999900524 ) ) ;
#13300=CARTESIAN_POINT ( 'NONE',  ( -22.49917142882856069, 22.89791325974001879, 3.749999999999900080 ) ) ;
#13371=DIRECTION ( 'NONE',  ( 2.982858504489139758E-17, -2.441916418604790135E-15, -1.000000000000000000 ) ) ;
#13380=DIRECTION ( 'NONE',  ( 0.000000000000000000, 0.000000000000000000, 1.000000000000000000 ) ) ;
#13416=CARTESIAN_POINT ( 'NONE',  ( -22.49917142882856069, 22.89791325974001879, 2.499999999999900524 ) ) ;
#13593=ORIENTED_EDGE ( 'NONE', *, *, #11641, .T. ) ;
#13830=EDGE_CURVE ( 'NONE', #8186, #8149, #3700, .T. ) ;
#13886=CARTESIAN_POINT ( 'NONE',  ( -19.99975861755300244, 22.95209442650120124, 3.749999999999900080 ) ) ;
#14096=CARTESIAN_POINT ( 'NONE',  ( -16.50058068176721804, 23.02794805996685668, 2.499999999999900524 ) ) ;
#14142=AXIS2_PLACEMENT_3D ( 'NONE', #13886, #8430, #6772 ) ;
#14308=AXIS2_PLACEMENT_3D ( 'NONE', #2174, #9312, #262 ) ;
#14353=ORIENTED_EDGE ( 'NONE', *, *, #22429, .F. ) ;
#14374=DIRECTION ( 'NONE',  ( -2.982858504489139758E-17, 2.441916418604790135E-15, 1.000000000000000000 ) ) ;
#14420=FACE_OUTER_BOUND ( 'NONE', #7968, .T. ) ;
#14474=ORIENTED_EDGE ( 'NONE', *, *, #18006, .F. ) ;
#14538=ORIENTED_EDGE ( 'NONE', *, *, #11506, .T. ) ;
#14590=DIRECTION ( 'NONE',  ( -0.9997651245102238127, -0.02167246670447303680, 0.000000000000000000 ) ) ;
#14658=DIRECTION ( 'NONE',  ( -0.9997651245102240347, -0.02167246670447264822, 0.000000000000000000 ) ) ;
#15067=CARTESIAN_POINT ( 'NONE',  ( -17.50034580627744063, 23.00627559326238369, 2.499999999999900524 ) ) ;
#15187=DIRECTION ( 'NONE',  ( 9.412241839989958199E-48, -1.000000000000000000, 2.441916418604790135E-15 ) ) ;
#15422=FACE_OUTER_BOUND ( 'NONE', #532, .T. ) ;
#15467=DIRECTION ( 'NONE',  ( 2.982858504489139758E-17, -2.441916418604790135E-15, -1.000000000000000000 ) ) ;
#15628=EDGE_LOOP ( 'NONE', ( #14538, #11809 ) ) ;
#15668=ORIENTED_EDGE ( 'NONE', *, *, #3312, .F. ) ;
#15789=CARTESIAN_POINT ( 'NONE',  ( -23.49893655333878684, 22.87624079303554581, 4.999999999999900524 ) ) ;
#16128=DIRECTION ( 'NONE',  ( -2.982858504489139758E-17, 2.441916418604790135E-15, 1.000000000000000000 ) ) ;
#16211=DIRECTION ( 'NONE',  ( -0.9997651245102240347, -0.02167246670447264822, 0.000000000000000000 ) ) ;
#16474=DIRECTION ( 'NONE',  ( 2.982858504489139758E-17, -2.441916418604790135E-15, -1.000000000000000000 ) ) ;
#16483=EDGE_CURVE ( 'NONE', #6885, #20045, #12254, .T. ) ;
#16780=ADVANCED_FACE ( 'NONE', ( #15422 ), #9999, .F. ) ;
#16888=PRODUCT_DEFINITION_SHAPE ( 'NONE', 'NONE',  #13165 ) ;
#16981=AXIS2_PLACEMENT_3D ( 'NONE', #5521, #161, #16211 ) ;
#17215=FACE_OUTER_BOUND ( 'NONE', #19964, .T. ) ;
#17245=CIRCLE ( 'NONE', #7009, 3.500000000000001332 ) ;
#17443=ORIENTED_EDGE ( 'NONE', *, *, #3312, .T. ) ;
#17733=CARTESIAN_POINT ( 'NONE',  ( -16.50058068176721804, 23.02794805996685668, 3.749999999999900080 ) ) ;
#17763=CARTESIAN_POINT ( 'NONE',  ( -19.99975861755300244, 22.95209442650120124, 3.749999999999900080 ) ) ;
#17802=CARTESIAN_POINT ( 'NONE',  ( -19.99975861755300244, 22.95209442650120124, 2.499999999999900524 ) ) ;
#17955=CARTESIAN_POINT ( 'NONE',  ( -19.99975861755300244, 22.95209442650120124, 4.999999999999900524 ) ) ;
#18006=EDGE_CURVE ( 'NONE', #20045, #6885, #17245, .T. ) ;
#18101=ADVANCED_FACE ( 'NONE', ( #12808 ), #7695, .T. ) ;
#18152=CARTESIAN_POINT ( 'NONE',  ( -19.99975861755300244, 22.95209442650120124, 4.999999999999900524 ) ) ;
#18164=ADVANCED_BREP_SHAPE_REPRESENTATION ( '', ( #9291, #12739 ), #210 ) ;
#18201=FACE_OUTER_BOUND ( 'NONE', #9815, .T. ) ;
#18585=( NAMED_UNIT ( * ) PLANE_ANGLE_UNIT ( ) SI_UNIT ( $, .RADIAN. ) );
#18937=CARTESIAN_POINT ( 'NONE',  ( -17.50034580627744063, 23.00627559326238369, 3.749999999999900080 ) ) ;
#19202=ORIENTED_EDGE ( 'NONE', *, *, #20404, .F. ) ;
#19390=LINE ( 'NONE', #17733, #21372 ) ;
#19702=CARTESIAN_POINT ( 'NONE',  ( -23.49893655333878684, 22.87624079303554581, 2.499999999999900524 ) ) ;
#19724=ORIENTED_EDGE ( 'NONE', *, *, #12616, .F. ) ;
#19964=EDGE_LOOP ( 'NONE', ( #4772, #14474 ) ) ;
#20045=VERTEX_POINT ( 'NONE', #14096 ) ;
#20294=ORIENTED_EDGE ( 'NONE', *, *, #21093, .F. ) ;
#20404=EDGE_CURVE ( 'NONE', #5266, #10552, #6944, .T. ) ;
#20467=DIRECTION ( 'NONE',  ( 2.982858504489129897E-17, -2.441916418604790135E-15, -1.000000000000000000 ) ) ;
#20762=PLANE ( 'NONE',  #21722 ) ;
#20768=DIRECTION ( 'NONE',  ( 2.982858504489139758E-17, -2.441916418604790135E-15, -1.000000000000000000 ) ) ;
#21013=PLANE ( 'NONE',  #3289 ) ;
#21093=EDGE_CURVE ( 'NONE', #10552, #20045, #19390, .T. ) ;
#21230=DIRECTION ( 'NONE',  ( -0.9997651245102238127, -0.02167246670447303680, 0.000000000000000000 ) ) ;
#21372=VECTOR ( 'NONE', #15467, 1000.000000000000000 ) ;
#21435=DIRECTION ( 'NONE',  ( 2.982858504489129897E-17, -2.441916418604790135E-15, -1.000000000000000000 ) ) ;
#21492=DIRECTION ( 'NONE',  ( -0.9997651245102240347, -0.02167246670447264822, 0.000000000000000000 ) ) ;
#21531=ORIENTED_EDGE ( 'NONE', *, *, #11506, .F. ) ;
#21722=AXIS2_PLACEMENT_3D ( 'NONE', #6394, #4382, #11650 ) ;
#21842=CARTESIAN_POINT ( 'NONE',  ( -19.99975861755300244, 22.95209442650120124, 2.499999999999900524 ) ) ;
#22047=CARTESIAN_POINT ( 'NONE',  ( -19.99975861755300244, 22.95209442650120124, 3.749999999999900080 ) ) ;
#22257=AXIS2_PLACEMENT_3D ( 'NONE', #13234, #20467, #5624 ) ;
#22427=CARTESIAN_POINT ( 'NONE',  ( -23.49893655333878684, 22.87624079303554581, 3.749999999999900080 ) ) ;
#22429=EDGE_CURVE ( 'NONE', #1608, #1750, #7497, .T. ) ;
#22678=AXIS2_PLACEMENT_3D ( 'NONE', #8487, #10156, #8355 ) ;
#22773=LINE ( 'NONE', #22427, #5551 ) ;
#22871=ORIENTED_EDGE ( 'NONE', *, *, #3012, .F. ) ;
#22994=VECTOR ( 'NONE', #9921, 1000.000000000000000 ) ;
#23412=CIRCLE ( 'NONE', #22678, 2.500000000000000000 ) ;
#23529=COLOUR_RGB('Sky Blue', 0.31764706, 0.68627451, 0.89019608);
#23530=FILL_AREA_STYLE_COLOUR('',#23529);
#23531=FILL_AREA_STYLE('',(#23530));
#23532=SURFACE_STYLE_FILL_AREA(#23531);
#23533=SURFACE_SIDE_STYLE('',(#23532));
#23534=SURFACE_STYLE_USAGE(.BOTH.,#23533);
#23535=PRESENTATION_STYLE_ASSIGNMENT((#23534));
#23617=STYLED_ITEM('',(#23535),#9291);
#23618=MECHANICAL_DESIGN_GEOMETRIC_PRESENTATION_REPRESENTATION('',(#23617),#210);
ENDSEC;
END-ISO-10303-21;
